ISO-10303-21;
HEADER;
/* Generated by software containing ST-Developer
 * from STEP Tools, Inc. (www.steptools.com) 
 */

FILE_DESCRIPTION(
/* description */ ('STEP AP214'),
/* implementation_level */ '2;1');

FILE_NAME(
/* name */ 'PUR-HW-4059.step',
/* time_stamp */ '2026-10-07T12:49:37-07:00',
/* author */ (''),
/* organization */ (''),
/* preprocessor_version */ 'ST-DEVELOPER v20.2',
/* originating_system */ 'Autodesk Translation Framework v15.15.0.0',
/* authorisation */ '');

FILE_SCHEMA (('AUTOMOTIVE_DESIGN { 1 0 10303 214 3 1 1 }'));
ENDSEC;

DATA;
#10=MECHANICAL_DESIGN_GEOMETRIC_PRESENTATION_REPRESENTATION('',(#295),#33016);
#241=SHAPE_REPRESENTATION_RELATIONSHIP('SRR','None',#33134,#268);
#268=ADVANCED_BREP_SHAPE_REPRESENTATION('',(#326),#32995);
#295=STYLED_ITEM('',(#33287),#326);
#326=MANIFOLD_SOLID_BREP('Body1',#9950);
#387=TOROIDAL_SURFACE('',#10700,8.55,1.65);
#1269=FACE_OUTER_BOUND('',#1847,.T.);
#1847=EDGE_LOOP('',(#7724,#7725,#7726,#7727));
#2396=CIRCLE('',#10701,1.65);
#2397=CIRCLE('',#10702,6.9);
#4525=VERTEX_POINT('',#21089);
#5675=EDGE_CURVE('',#4525,#4525,#2396,.T.);
#5676=EDGE_CURVE('',#4525,#4525,#2397,.T.);
#7724=ORIENTED_EDGE('',*,*,#5675,.F.);
#7725=ORIENTED_EDGE('',*,*,#5676,.T.);
#7726=ORIENTED_EDGE('',*,*,#5675,.T.);
#7727=ORIENTED_EDGE('',*,*,#5676,.F.);
#9635=ADVANCED_FACE('',(#1269),#387,.T.);
#9950=CLOSED_SHELL('',(#9635));
#10699=AXIS2_PLACEMENT_3D('',#21087,#12511,#12512);
#10700=AXIS2_PLACEMENT_3D('',#21088,#12513,#12514);
#10701=AXIS2_PLACEMENT_3D('',#21090,#12515,#12516);
#10702=AXIS2_PLACEMENT_3D('',#21091,#12517,#12518);
#12511=DIRECTION('axis',(0.,0.,1.));
#12512=DIRECTION('refdir',(1.,0.,0.));
#12513=DIRECTION('center_axis',(0.,1.,0.));
#12514=DIRECTION('ref_axis',(0.,0.,1.));
#12515=DIRECTION('center_axis',(-1.,0.,1.22464679914735E-16));
#12516=DIRECTION('ref_axis',(-1.22464679914735E-16,0.,-1.));
#12517=DIRECTION('center_axis',(0.,-1.,0.));
#12518=DIRECTION('ref_axis',(0.,0.,1.));
#21087=CARTESIAN_POINT('',(0.,0.,0.));
#21088=CARTESIAN_POINT('Origin',(0.,0.,0.));
#21089=CARTESIAN_POINT('',(-8.45006291411674E-16,2.02066721859313E-16,-6.9));
#21090=CARTESIAN_POINT('Origin',(-1.04707301327099E-15,0.,-8.55));
#21091=CARTESIAN_POINT('Origin',(0.,-2.02066721859313E-16,0.));
#32963=UNCERTAINTY_MEASURE_WITH_UNIT(LENGTH_MEASURE(0.01),#33017,
'DISTANCE_ACCURACY_VALUE',
'Maximum model space distance between geometric entities at asserted c
onnectivities');
#32984=UNCERTAINTY_MEASURE_WITH_UNIT(LENGTH_MEASURE(0.01),#33017,
'DISTANCE_ACCURACY_VALUE',
'Maximum model space distance between geometric entities at asserted c
onnectivities');
#32995=(
GEOMETRIC_REPRESENTATION_CONTEXT(3)
GLOBAL_UNCERTAINTY_ASSIGNED_CONTEXT((#32963))
GLOBAL_UNIT_ASSIGNED_CONTEXT((#33017,#33019,#33020))
REPRESENTATION_CONTEXT('','3D')
);
#33016=(
GEOMETRIC_REPRESENTATION_CONTEXT(3)
GLOBAL_UNCERTAINTY_ASSIGNED_CONTEXT((#32984))
GLOBAL_UNIT_ASSIGNED_CONTEXT((#33017,#33019,#33020))
REPRESENTATION_CONTEXT('','3D')
);
#33017=(
LENGTH_UNIT()
NAMED_UNIT(*)
SI_UNIT(.MILLI.,.METRE.)
);
#33019=(
NAMED_UNIT(*)
PLANE_ANGLE_UNIT()
SI_UNIT($,.RADIAN.)
);
#33020=(
NAMED_UNIT(*)
SI_UNIT($,.STERADIAN.)
SOLID_ANGLE_UNIT()
);
#33031=SHAPE_DEFINITION_REPRESENTATION(#33070,#33134);
#33070=PRODUCT_DEFINITION_SHAPE('',$,#33166);
#33134=SHAPE_REPRESENTATION('',(#10699),#32995);
#33155=PRODUCT_DEFINITION_CONTEXT('part definition',#33250,'design');
#33166=PRODUCT_DEFINITION(
'BO26-002_O Ring_PUR-HW-4059_20.4 OD x 13.8 ID x 3.3 T','PUR-HW-4059',#33197,
#33155);
#33197=PRODUCT_DEFINITION_FORMATION('',$,#33262);
#33250=APPLICATION_CONTEXT(
'Core Data for Automotive Mechanical Design Process');
#33251=PRODUCT_CONTEXT('part definition',#33250,'mechanical');
#33262=PRODUCT('BO26-002_O Ring_PUR-HW-4059_20.4 OD x 13.8 ID x 3.3 T',
'PUR-HW-4059',$,(#33251));
#33287=PRESENTATION_STYLE_ASSIGNMENT((#33294));
#33294=SURFACE_STYLE_USAGE(.BOTH.,#33301);
#33301=SURFACE_SIDE_STYLE('',(#33308));
#33308=SURFACE_STYLE_FILL_AREA(#33315);
#33315=FILL_AREA_STYLE('Opaque(76,76,76)',(#33322));
#33322=FILL_AREA_STYLE_COLOUR('Opaque(76,76,76)',#33329);
#33329=COLOUR_RGB('Opaque(76,76,76)', 0.31764706, 0.68627451, 0.89019608);
ENDSEC;
END-ISO-10303-21;
